ISO-10303-21;
HEADER;
/* Generated by software containing ST-Developer
 * from STEP Tools, Inc. (www.steptools.com) 
 */

FILE_DESCRIPTION(
/* description */ ('PAT-072'),
/* implementation_level */ '2;1');

FILE_NAME(
/* name */ 'Hex Pipe Nipple - 1-4 Inch Tapered Pipe Thread.step',
/* time_stamp */ '2026-10-29T20:11:56-07:00',
/* author */ (''),
/* organization */ (''),
/* preprocessor_version */ 'ST-DEVELOPER v20.2',
/* originating_system */ 'Autodesk Translation Framework v15.17.0.0',
/* authorisation */ '');

FILE_SCHEMA (('AUTOMOTIVE_DESIGN { 1 0 10303 214 3 1 1 }'));
ENDSEC;

DATA;
#10=MECHANICAL_DESIGN_GEOMETRIC_PRESENTATION_REPRESENTATION('',(#366),#11432);
#214=CONICAL_SURFACE('',#7177,0.645,0.785398163397448);
#215=CONICAL_SURFACE('',#7180,0.645,0.785398163397448);
#294=SHAPE_REPRESENTATION_RELATIONSHIP('SRR','None',#11599,#330);
#330=ADVANCED_BREP_SHAPE_REPRESENTATION('',(#401),#11430);
#366=STYLED_ITEM('',(#11812),#401);
#401=MANIFOLD_SOLID_BREP('Body1',#6102);
#565=FACE_BOUND('',#1672,.T.);
#566=FACE_BOUND('',#1674,.T.);
#567=FACE_BOUND('',#1683,.T.);
#568=FACE_BOUND('',#1688,.T.);
#775=PLANE('',#7162);
#776=PLANE('',#7164);
#777=PLANE('',#7166);
#778=PLANE('',#7167);
#779=PLANE('',#7168);
#780=PLANE('',#7169);
#781=PLANE('',#7170);
#782=PLANE('',#7171);
#783=PLANE('',#7174);
#784=PLANE('',#7182);
#1136=FACE_OUTER_BOUND('',#1671,.T.);
#1137=FACE_OUTER_BOUND('',#1673,.T.);
#1138=FACE_OUTER_BOUND('',#1675,.T.);
#1139=FACE_OUTER_BOUND('',#1676,.T.);
#1140=FACE_OUTER_BOUND('',#1677,.T.);
#1141=FACE_OUTER_BOUND('',#1678,.T.);
#1142=FACE_OUTER_BOUND('',#1679,.T.);
#1143=FACE_OUTER_BOUND('',#1680,.T.);
#1144=FACE_OUTER_BOUND('',#1681,.T.);
#1145=FACE_OUTER_BOUND('',#1682,.T.);
#1146=FACE_OUTER_BOUND('',#1684,.T.);
#1147=FACE_OUTER_BOUND('',#1685,.T.);
#1148=FACE_OUTER_BOUND('',#1686,.T.);
#1149=FACE_OUTER_BOUND('',#1687,.T.);
#1150=FACE_OUTER_BOUND('',#1689,.T.);
#1671=EDGE_LOOP('',(#5432,#5433,#5434,#5435,#5436,#5437));
#1672=EDGE_LOOP('',(#5438));
#1673=EDGE_LOOP('',(#5439,#5440,#5441,#5442,#5443,#5444));
#1674=EDGE_LOOP('',(#5445));
#1675=EDGE_LOOP('',(#5446,#5447,#5448,#5449));
#1676=EDGE_LOOP('',(#5450,#5451,#5452,#5453));
#1677=EDGE_LOOP('',(#5454,#5455,#5456,#5457));
#1678=EDGE_LOOP('',(#5458,#5459,#5460,#5461));
#1679=EDGE_LOOP('',(#5462,#5463,#5464,#5465));
#1680=EDGE_LOOP('',(#5466,#5467,#5468,#5469));
#1681=EDGE_LOOP('',(#5470,#5471,#5472,#5473));
#1682=EDGE_LOOP('',(#5474));
#1683=EDGE_LOOP('',(#5475));
#1684=EDGE_LOOP('',(#5476,#5477,#5478,#5479));
#1685=EDGE_LOOP('',(#5480,#5481,#5482,#5483));
#1686=EDGE_LOOP('',(#5484,#5485,#5486,#5487));
#1687=EDGE_LOOP('',(#5488));
#1688=EDGE_LOOP('',(#5489));
#1689=EDGE_LOOP('',(#5490,#5491,#5492,#5493));
#2080=LINE('',#11174,#2499);
#2081=LINE('',#11176,#2500);
#2082=LINE('',#11178,#2501);
#2083=LINE('',#11180,#2502);
#2084=LINE('',#11182,#2503);
#2085=LINE('',#11183,#2504);
#2086=LINE('',#11189,#2505);
#2087=LINE('',#11191,#2506);
#2088=LINE('',#11193,#2507);
#2089=LINE('',#11195,#2508);
#2090=LINE('',#11197,#2509);
#2091=LINE('',#11198,#2510);
#2092=LINE('',#11202,#2511);
#2093=LINE('',#11203,#2512);
#2094=LINE('',#11205,#2513);
#2095=LINE('',#11207,#2514);
#2096=LINE('',#11209,#2515);
#2097=LINE('',#11211,#2516);
#2098=LINE('',#11215,#2517);
#2099=LINE('',#11223,#2518);
#2100=LINE('',#11227,#2519);
#2101=LINE('',#11231,#2520);
#2102=LINE('',#11236,#2521);
#2499=VECTOR('',#8953,1.);
#2500=VECTOR('',#8954,1.);
#2501=VECTOR('',#8955,1.);
#2502=VECTOR('',#8956,1.);
#2503=VECTOR('',#8957,1.);
#2504=VECTOR('',#8958,1.);
#2505=VECTOR('',#8963,1.);
#2506=VECTOR('',#8964,1.);
#2507=VECTOR('',#8965,1.);
#2508=VECTOR('',#8966,1.);
#2509=VECTOR('',#8967,1.);
#2510=VECTOR('',#8968,1.);
#2511=VECTOR('',#8973,1.);
#2512=VECTOR('',#8974,1.);
#2513=VECTOR('',#8977,1.);
#2514=VECTOR('',#8980,1.);
#2515=VECTOR('',#8983,1.);
#2516=VECTOR('',#8986,1.);
#2517=VECTOR('',#8991,0.685);
#2518=VECTOR('',#9002,0.645);
#2519=VECTOR('',#9007,0.685);
#2520=VECTOR('',#9012,0.645);
#2521=VECTOR('',#9019,0.46);
#2820=CIRCLE('',#7163,0.685);
#2821=CIRCLE('',#7165,0.685);
#2822=CIRCLE('',#7173,0.685);
#2823=CIRCLE('',#7175,0.605);
#2824=CIRCLE('',#7176,0.46);
#2825=CIRCLE('',#7179,0.685);
#2826=CIRCLE('',#7181,0.605);
#2827=CIRCLE('',#7183,0.46);
#3283=VERTEX_POINT('',#11172);
#3284=VERTEX_POINT('',#11173);
#3285=VERTEX_POINT('',#11175);
#3286=VERTEX_POINT('',#11177);
#3287=VERTEX_POINT('',#11179);
#3288=VERTEX_POINT('',#11181);
#3289=VERTEX_POINT('',#11184);
#3290=VERTEX_POINT('',#11187);
#3291=VERTEX_POINT('',#11188);
#3292=VERTEX_POINT('',#11190);
#3293=VERTEX_POINT('',#11192);
#3294=VERTEX_POINT('',#11194);
#3295=VERTEX_POINT('',#11196);
#3296=VERTEX_POINT('',#11199);
#3297=VERTEX_POINT('',#11214);
#3298=VERTEX_POINT('',#11218);
#3299=VERTEX_POINT('',#11220);
#3300=VERTEX_POINT('',#11225);
#3301=VERTEX_POINT('',#11229);
#3302=VERTEX_POINT('',#11233);
#4005=EDGE_CURVE('',#3283,#3284,#2080,.T.);
#4006=EDGE_CURVE('',#3284,#3285,#2081,.T.);
#4007=EDGE_CURVE('',#3285,#3286,#2082,.T.);
#4008=EDGE_CURVE('',#3286,#3287,#2083,.T.);
#4009=EDGE_CURVE('',#3287,#3288,#2084,.T.);
#4010=EDGE_CURVE('',#3288,#3283,#2085,.T.);
#4011=EDGE_CURVE('',#3289,#3289,#2820,.T.);
#4012=EDGE_CURVE('',#3290,#3291,#2086,.T.);
#4013=EDGE_CURVE('',#3291,#3292,#2087,.T.);
#4014=EDGE_CURVE('',#3292,#3293,#2088,.T.);
#4015=EDGE_CURVE('',#3293,#3294,#2089,.T.);
#4016=EDGE_CURVE('',#3294,#3295,#2090,.T.);
#4017=EDGE_CURVE('',#3295,#3290,#2091,.T.);
#4018=EDGE_CURVE('',#3296,#3296,#2821,.T.);
#4019=EDGE_CURVE('',#3290,#3284,#2092,.T.);
#4020=EDGE_CURVE('',#3285,#3295,#2093,.T.);
#4021=EDGE_CURVE('',#3286,#3294,#2094,.T.);
#4022=EDGE_CURVE('',#3287,#3293,#2095,.T.);
#4023=EDGE_CURVE('',#3288,#3292,#2096,.T.);
#4024=EDGE_CURVE('',#3283,#3291,#2097,.T.);
#4025=EDGE_CURVE('',#3296,#3297,#2098,.T.);
#4026=EDGE_CURVE('',#3297,#3297,#2822,.T.);
#4027=EDGE_CURVE('',#3298,#3298,#2823,.T.);
#4028=EDGE_CURVE('',#3299,#3299,#2824,.T.);
#4029=EDGE_CURVE('',#3297,#3298,#2099,.T.);
#4030=EDGE_CURVE('',#3300,#3300,#2825,.T.);
#4031=EDGE_CURVE('',#3300,#3289,#2100,.T.);
#4032=EDGE_CURVE('',#3301,#3301,#2826,.T.);
#4033=EDGE_CURVE('',#3301,#3300,#2101,.T.);
#4034=EDGE_CURVE('',#3302,#3302,#2827,.T.);
#4035=EDGE_CURVE('',#3302,#3299,#2102,.T.);
#5432=ORIENTED_EDGE('',*,*,#4005,.T.);
#5433=ORIENTED_EDGE('',*,*,#4006,.T.);
#5434=ORIENTED_EDGE('',*,*,#4007,.T.);
#5435=ORIENTED_EDGE('',*,*,#4008,.T.);
#5436=ORIENTED_EDGE('',*,*,#4009,.T.);
#5437=ORIENTED_EDGE('',*,*,#4010,.T.);
#5438=ORIENTED_EDGE('',*,*,#4011,.F.);
#5439=ORIENTED_EDGE('',*,*,#4012,.T.);
#5440=ORIENTED_EDGE('',*,*,#4013,.T.);
#5441=ORIENTED_EDGE('',*,*,#4014,.T.);
#5442=ORIENTED_EDGE('',*,*,#4015,.T.);
#5443=ORIENTED_EDGE('',*,*,#4016,.T.);
#5444=ORIENTED_EDGE('',*,*,#4017,.T.);
#5445=ORIENTED_EDGE('',*,*,#4018,.F.);
#5446=ORIENTED_EDGE('',*,*,#4019,.F.);
#5447=ORIENTED_EDGE('',*,*,#4017,.F.);
#5448=ORIENTED_EDGE('',*,*,#4020,.F.);
#5449=ORIENTED_EDGE('',*,*,#4006,.F.);
#5450=ORIENTED_EDGE('',*,*,#4020,.T.);
#5451=ORIENTED_EDGE('',*,*,#4016,.F.);
#5452=ORIENTED_EDGE('',*,*,#4021,.F.);
#5453=ORIENTED_EDGE('',*,*,#4007,.F.);
#5454=ORIENTED_EDGE('',*,*,#4021,.T.);
#5455=ORIENTED_EDGE('',*,*,#4015,.F.);
#5456=ORIENTED_EDGE('',*,*,#4022,.F.);
#5457=ORIENTED_EDGE('',*,*,#4008,.F.);
#5458=ORIENTED_EDGE('',*,*,#4022,.T.);
#5459=ORIENTED_EDGE('',*,*,#4014,.F.);
#5460=ORIENTED_EDGE('',*,*,#4023,.F.);
#5461=ORIENTED_EDGE('',*,*,#4009,.F.);
#5462=ORIENTED_EDGE('',*,*,#4023,.T.);
#5463=ORIENTED_EDGE('',*,*,#4013,.F.);
#5464=ORIENTED_EDGE('',*,*,#4024,.F.);
#5465=ORIENTED_EDGE('',*,*,#4010,.F.);
#5466=ORIENTED_EDGE('',*,*,#4024,.T.);
#5467=ORIENTED_EDGE('',*,*,#4012,.F.);
#5468=ORIENTED_EDGE('',*,*,#4019,.T.);
#5469=ORIENTED_EDGE('',*,*,#4005,.F.);
#5470=ORIENTED_EDGE('',*,*,#4018,.T.);
#5471=ORIENTED_EDGE('',*,*,#4025,.T.);
#5472=ORIENTED_EDGE('',*,*,#4026,.T.);
#5473=ORIENTED_EDGE('',*,*,#4025,.F.);
#5474=ORIENTED_EDGE('',*,*,#4027,.F.);
#5475=ORIENTED_EDGE('',*,*,#4028,.T.);
#5476=ORIENTED_EDGE('',*,*,#4026,.F.);
#5477=ORIENTED_EDGE('',*,*,#4029,.T.);
#5478=ORIENTED_EDGE('',*,*,#4027,.T.);
#5479=ORIENTED_EDGE('',*,*,#4029,.F.);
#5480=ORIENTED_EDGE('',*,*,#4030,.F.);
#5481=ORIENTED_EDGE('',*,*,#4031,.T.);
#5482=ORIENTED_EDGE('',*,*,#4011,.T.);
#5483=ORIENTED_EDGE('',*,*,#4031,.F.);
#5484=ORIENTED_EDGE('',*,*,#4032,.F.);
#5485=ORIENTED_EDGE('',*,*,#4033,.T.);
#5486=ORIENTED_EDGE('',*,*,#4030,.T.);
#5487=ORIENTED_EDGE('',*,*,#4033,.F.);
#5488=ORIENTED_EDGE('',*,*,#4032,.T.);
#5489=ORIENTED_EDGE('',*,*,#4034,.F.);
#5490=ORIENTED_EDGE('',*,*,#4034,.T.);
#5491=ORIENTED_EDGE('',*,*,#4035,.T.);
#5492=ORIENTED_EDGE('',*,*,#4028,.F.);
#5493=ORIENTED_EDGE('',*,*,#4035,.F.);
#5690=CYLINDRICAL_SURFACE('',#7172,0.685);
#5691=CYLINDRICAL_SURFACE('',#7178,0.685);
#5692=CYLINDRICAL_SURFACE('',#7184,0.46);
#6035=ADVANCED_FACE('',(#1136,#565),#775,.F.);
#6036=ADVANCED_FACE('',(#1137,#566),#776,.T.);
#6037=ADVANCED_FACE('',(#1138),#777,.T.);
#6038=ADVANCED_FACE('',(#1139),#778,.T.);
#6039=ADVANCED_FACE('',(#1140),#779,.T.);
#6040=ADVANCED_FACE('',(#1141),#780,.T.);
#6041=ADVANCED_FACE('',(#1142),#781,.T.);
#6042=ADVANCED_FACE('',(#1143),#782,.T.);
#6043=ADVANCED_FACE('',(#1144),#5690,.T.);
#6044=ADVANCED_FACE('',(#1145,#567),#783,.T.);
#6045=ADVANCED_FACE('',(#1146),#214,.T.);
#6046=ADVANCED_FACE('',(#1147),#5691,.T.);
#6047=ADVANCED_FACE('',(#1148),#215,.T.);
#6048=ADVANCED_FACE('',(#1149,#568),#784,.T.);
#6049=ADVANCED_FACE('',(#1150),#5692,.F.);
#6102=CLOSED_SHELL('',(#6035,#6036,#6037,#6038,#6039,#6040,#6041,#6042,
#6043,#6044,#6045,#6046,#6047,#6048,#6049));
#7161=AXIS2_PLACEMENT_3D('',#11170,#8949,#8950);
#7162=AXIS2_PLACEMENT_3D('',#11171,#8951,#8952);
#7163=AXIS2_PLACEMENT_3D('',#11185,#8959,#8960);
#7164=AXIS2_PLACEMENT_3D('',#11186,#8961,#8962);
#7165=AXIS2_PLACEMENT_3D('',#11200,#8969,#8970);
#7166=AXIS2_PLACEMENT_3D('',#11201,#8971,#8972);
#7167=AXIS2_PLACEMENT_3D('',#11204,#8975,#8976);
#7168=AXIS2_PLACEMENT_3D('',#11206,#8978,#8979);
#7169=AXIS2_PLACEMENT_3D('',#11208,#8981,#8982);
#7170=AXIS2_PLACEMENT_3D('',#11210,#8984,#8985);
#7171=AXIS2_PLACEMENT_3D('',#11212,#8987,#8988);
#7172=AXIS2_PLACEMENT_3D('',#11213,#8989,#8990);
#7173=AXIS2_PLACEMENT_3D('',#11216,#8992,#8993);
#7174=AXIS2_PLACEMENT_3D('',#11217,#8994,#8995);
#7175=AXIS2_PLACEMENT_3D('',#11219,#8996,#8997);
#7176=AXIS2_PLACEMENT_3D('',#11221,#8998,#8999);
#7177=AXIS2_PLACEMENT_3D('',#11222,#9000,#9001);
#7178=AXIS2_PLACEMENT_3D('',#11224,#9003,#9004);
#7179=AXIS2_PLACEMENT_3D('',#11226,#9005,#9006);
#7180=AXIS2_PLACEMENT_3D('',#11228,#9008,#9009);
#7181=AXIS2_PLACEMENT_3D('',#11230,#9010,#9011);
#7182=AXIS2_PLACEMENT_3D('',#11232,#9013,#9014);
#7183=AXIS2_PLACEMENT_3D('',#11234,#9015,#9016);
#7184=AXIS2_PLACEMENT_3D('',#11235,#9017,#9018);
#8949=DIRECTION('axis',(0.,0.,1.));
#8950=DIRECTION('refdir',(1.,0.,0.));
#8951=DIRECTION('center_axis',(0.,1.,0.));
#8952=DIRECTION('ref_axis',(1.,0.,0.));
#8953=DIRECTION('',(-0.5,0.,0.866025403784439));
#8954=DIRECTION('',(-1.,0.,-3.29650746237182E-16));
#8955=DIRECTION('',(-0.5,0.,-0.866025403784439));
#8956=DIRECTION('',(0.5,0.,-0.866025403784438));
#8957=DIRECTION('',(1.,0.,0.));
#8958=DIRECTION('',(0.5,0.,0.866025403784439));
#8959=DIRECTION('center_axis',(0.,-1.,0.));
#8960=DIRECTION('ref_axis',(1.,0.,0.));
#8961=DIRECTION('center_axis',(0.,1.,0.));
#8962=DIRECTION('ref_axis',(1.,0.,0.));
#8963=DIRECTION('',(0.5,0.,-0.866025403784439));
#8964=DIRECTION('',(-0.5,0.,-0.866025403784439));
#8965=DIRECTION('',(-1.,0.,0.));
#8966=DIRECTION('',(-0.5,0.,0.866025403784438));
#8967=DIRECTION('',(0.5,0.,0.866025403784439));
#8968=DIRECTION('',(1.,0.,3.29650746237182E-16));
#8969=DIRECTION('center_axis',(0.,1.,0.));
#8970=DIRECTION('ref_axis',(1.,0.,0.));
#8971=DIRECTION('center_axis',(-3.29650746237182E-16,0.,1.));
#8972=DIRECTION('ref_axis',(1.,0.,3.29650746237182E-16));
#8973=DIRECTION('',(0.,-1.,0.));
#8974=DIRECTION('',(0.,1.,0.));
#8975=DIRECTION('center_axis',(-0.866025403784439,0.,0.5));
#8976=DIRECTION('ref_axis',(0.5,0.,0.866025403784439));
#8977=DIRECTION('',(0.,1.,0.));
#8978=DIRECTION('center_axis',(-0.866025403784439,0.,-0.5));
#8979=DIRECTION('ref_axis',(-0.5,0.,0.866025403784439));
#8980=DIRECTION('',(0.,1.,0.));
#8981=DIRECTION('center_axis',(0.,0.,-1.));
#8982=DIRECTION('ref_axis',(-1.,0.,0.));
#8983=DIRECTION('',(0.,1.,0.));
#8984=DIRECTION('center_axis',(0.866025403784439,0.,-0.5));
#8985=DIRECTION('ref_axis',(-0.5,0.,-0.866025403784439));
#8986=DIRECTION('',(0.,1.,0.));
#8987=DIRECTION('center_axis',(0.866025403784439,0.,0.5));
#8988=DIRECTION('ref_axis',(0.5,0.,-0.866025403784439));
#8989=DIRECTION('center_axis',(0.,-1.,0.));
#8990=DIRECTION('ref_axis',(1.,0.,0.));
#8991=DIRECTION('',(0.,1.,0.));
#8992=DIRECTION('center_axis',(0.,-1.,0.));
#8993=DIRECTION('ref_axis',(1.,0.,0.));
#8994=DIRECTION('center_axis',(0.,1.,0.));
#8995=DIRECTION('ref_axis',(0.,0.,1.));
#8996=DIRECTION('center_axis',(0.,-1.,0.));
#8997=DIRECTION('ref_axis',(1.,0.,0.));
#8998=DIRECTION('center_axis',(0.,-1.,0.));
#8999=DIRECTION('ref_axis',(1.,0.,0.));
#9000=DIRECTION('center_axis',(0.,-1.,0.));
#9001=DIRECTION('ref_axis',(1.,0.,0.));
#9002=DIRECTION('',(0.707106781186547,0.707106781186548,8.65956056235493E-17));
#9003=DIRECTION('center_axis',(0.,-1.,0.));
#9004=DIRECTION('ref_axis',(1.,0.,0.));
#9005=DIRECTION('center_axis',(0.,-1.,0.));
#9006=DIRECTION('ref_axis',(1.,0.,0.));
#9007=DIRECTION('',(0.,1.,0.));
#9008=DIRECTION('center_axis',(0.,1.,0.));
#9009=DIRECTION('ref_axis',(1.,0.,0.));
#9010=DIRECTION('center_axis',(0.,-1.,0.));
#9011=DIRECTION('ref_axis',(1.,0.,0.));
#9012=DIRECTION('',(-0.707106781186547,0.707106781186548,-8.65956056235493E-17));
#9013=DIRECTION('center_axis',(0.,-1.,0.));
#9014=DIRECTION('ref_axis',(0.,0.,-1.));
#9015=DIRECTION('center_axis',(0.,-1.,0.));
#9016=DIRECTION('ref_axis',(1.,0.,0.));
#9017=DIRECTION('center_axis',(0.,-1.,0.));
#9018=DIRECTION('ref_axis',(1.,0.,0.));
#9019=DIRECTION('',(0.,1.,0.));
#11170=CARTESIAN_POINT('',(0.,0.,0.));
#11171=CARTESIAN_POINT('Origin',(0.,-0.4,0.));
#11172=CARTESIAN_POINT('',(1.01036297108185,-0.4,0.));
#11173=CARTESIAN_POINT('',(0.505181485540923,-0.4,0.875));
#11174=CARTESIAN_POINT('',(0.505181485540923,-0.4,0.875));
#11175=CARTESIAN_POINT('',(-0.505181485540923,-0.4,0.875));
#11176=CARTESIAN_POINT('',(-0.505181485540923,-0.4,0.875));
#11177=CARTESIAN_POINT('',(-1.01036297108185,-0.4,-1.23733777851239E-16));
#11178=CARTESIAN_POINT('',(-1.01036297108185,-0.4,-1.23733777851239E-16));
#11179=CARTESIAN_POINT('',(-0.505181485540922,-0.4,-0.875));
#11180=CARTESIAN_POINT('',(-0.505181485540922,-0.4,-0.875));
#11181=CARTESIAN_POINT('',(0.505181485540923,-0.4,-0.875));
#11182=CARTESIAN_POINT('',(0.505181485540923,-0.4,-0.875));
#11183=CARTESIAN_POINT('',(1.01036297108185,-0.4,0.));
#11184=CARTESIAN_POINT('',(-0.685,-0.4,-8.38883057415937E-17));
#11185=CARTESIAN_POINT('Origin',(0.,-0.4,0.));
#11186=CARTESIAN_POINT('Origin',(0.,0.4,0.));
#11187=CARTESIAN_POINT('',(0.505181485540923,0.4,0.875));
#11188=CARTESIAN_POINT('',(1.01036297108185,0.4,0.));
#11189=CARTESIAN_POINT('',(0.505181485540923,0.4,0.875));
#11190=CARTESIAN_POINT('',(0.505181485540923,0.4,-0.875));
#11191=CARTESIAN_POINT('',(1.01036297108185,0.4,0.));
#11192=CARTESIAN_POINT('',(-0.505181485540922,0.4,-0.875));
#11193=CARTESIAN_POINT('',(0.505181485540923,0.4,-0.875));
#11194=CARTESIAN_POINT('',(-1.01036297108185,0.4,-1.23733777851239E-16));
#11195=CARTESIAN_POINT('',(-0.505181485540922,0.4,-0.875));
#11196=CARTESIAN_POINT('',(-0.505181485540923,0.4,0.875));
#11197=CARTESIAN_POINT('',(-1.01036297108185,0.4,-1.23733777851239E-16));
#11198=CARTESIAN_POINT('',(-0.505181485540923,0.4,0.875));
#11199=CARTESIAN_POINT('',(-0.685,0.4,8.38883057415937E-17));
#11200=CARTESIAN_POINT('Origin',(0.,0.4,0.));
#11201=CARTESIAN_POINT('Origin',(-0.505181485540923,0.,0.875));
#11202=CARTESIAN_POINT('',(0.505181485540923,0.,0.875));
#11203=CARTESIAN_POINT('',(-0.505181485540923,0.,0.875));
#11204=CARTESIAN_POINT('Origin',(-1.01036297108185,0.,-1.23733777851239E-16));
#11205=CARTESIAN_POINT('',(-1.01036297108185,0.,-1.23733777851239E-16));
#11206=CARTESIAN_POINT('Origin',(-0.505181485540922,0.,-0.875));
#11207=CARTESIAN_POINT('',(-0.505181485540922,0.,-0.875));
#11208=CARTESIAN_POINT('Origin',(0.505181485540923,0.,-0.875));
#11209=CARTESIAN_POINT('',(0.505181485540923,0.,-0.875));
#11210=CARTESIAN_POINT('Origin',(1.01036297108185,0.,0.));
#11211=CARTESIAN_POINT('',(1.01036297108185,0.,0.));
#11212=CARTESIAN_POINT('Origin',(0.505181485540923,0.,0.875));
#11213=CARTESIAN_POINT('Origin',(0.,0.,0.));
#11214=CARTESIAN_POINT('',(-0.685,1.82,-8.38883057415937E-17));
#11215=CARTESIAN_POINT('',(-0.685,0.,-8.38883057415937E-17));
#11216=CARTESIAN_POINT('Origin',(0.,1.82,0.));
#11217=CARTESIAN_POINT('Origin',(0.605,1.9,0.));
#11218=CARTESIAN_POINT('',(-0.605,1.9,-7.40911313484149E-17));
#11219=CARTESIAN_POINT('Origin',(0.,1.9,0.));
#11220=CARTESIAN_POINT('',(-0.46,1.9,-5.63337527607782E-17));
#11221=CARTESIAN_POINT('Origin',(0.,1.9,0.));
#11222=CARTESIAN_POINT('Origin',(0.,1.86,0.));
#11223=CARTESIAN_POINT('',(-0.645,1.86,-7.89897185450043E-17));
#11224=CARTESIAN_POINT('Origin',(0.,0.,0.));
#11225=CARTESIAN_POINT('',(-0.685,-1.82,-8.38883057415937E-17));
#11226=CARTESIAN_POINT('Origin',(0.,-1.82,0.));
#11227=CARTESIAN_POINT('',(-0.685,0.,-8.38883057415937E-17));
#11228=CARTESIAN_POINT('Origin',(0.,-1.86,0.));
#11229=CARTESIAN_POINT('',(-0.605,-1.9,-7.40911313484149E-17));
#11230=CARTESIAN_POINT('Origin',(0.,-1.9,0.));
#11231=CARTESIAN_POINT('',(-0.645,-1.86,-7.89897185450043E-17));
#11232=CARTESIAN_POINT('Origin',(0.46,-1.9,0.));
#11233=CARTESIAN_POINT('',(-0.46,-1.9,-5.63337527607782E-17));
#11234=CARTESIAN_POINT('Origin',(0.,-1.9,0.));
#11235=CARTESIAN_POINT('Origin',(0.,0.,0.));
#11236=CARTESIAN_POINT('',(-0.46,0.,-5.63337527607782E-17));
#11391=UNCERTAINTY_MEASURE_WITH_UNIT(LENGTH_MEASURE(0.001),#11433,
'DISTANCE_ACCURACY_VALUE',
'Maximum model space distance between geometric entities at asserted c
onnectivities');
#11393=UNCERTAINTY_MEASURE_WITH_UNIT(LENGTH_MEASURE(0.001),#11433,
'DISTANCE_ACCURACY_VALUE',
'Maximum model space distance between geometric entities at asserted c
onnectivities');
#11430=(
GEOMETRIC_REPRESENTATION_CONTEXT(3)
GLOBAL_UNCERTAINTY_ASSIGNED_CONTEXT((#11391))
GLOBAL_UNIT_ASSIGNED_CONTEXT((#11433,#11435,#11436))
REPRESENTATION_CONTEXT('','3D')
);
#11432=(
GEOMETRIC_REPRESENTATION_CONTEXT(3)
GLOBAL_UNCERTAINTY_ASSIGNED_CONTEXT((#11393))
GLOBAL_UNIT_ASSIGNED_CONTEXT((#11433,#11435,#11436))
REPRESENTATION_CONTEXT('','3D')
);
#11433=(
LENGTH_UNIT()
NAMED_UNIT(*)
SI_UNIT(.CENTI.,.METRE.)
);
#11435=(
NAMED_UNIT(*)
PLANE_ANGLE_UNIT()
SI_UNIT($,.RADIAN.)
);
#11436=(
NAMED_UNIT(*)
SI_UNIT($,.STERADIAN.)
SOLID_ANGLE_UNIT()
);
#11473=SHAPE_DEFINITION_REPRESENTATION(#11513,#11599);
#11513=PRODUCT_DEFINITION_SHAPE('',$,#11638);
#11599=SHAPE_REPRESENTATION('',(#7161),#11430);
#11601=PRODUCT_DEFINITION_CONTEXT('part definition',#11717,'design');
#11638=PRODUCT_DEFINITION('Hex Pipe Nipple - 1-4 Inch Tapered Pipe Thread',
'Hex Pipe Nipple - 1-4 Inch Tapered Pipe Thread',#11676,#11601);
#11676=PRODUCT_DEFINITION_FORMATION('',$,#11755);
#11717=APPLICATION_CONTEXT(
'Core Data for Automotive Mechanical Design Process');
#11718=PRODUCT_CONTEXT('part definition',#11717,'mechanical');
#11755=PRODUCT('Hex Pipe Nipple - 1-4 Inch Tapered Pipe Thread',
'Hex Pipe Nipple - 1-4 Inch Tapered Pipe Thread',
'Hex Pipe Nipple - 1-4 Inch Tapered Pipe Thread',(#11718));
#11806=COLOUR_RGB('Sky Blue',0.24,0.69,0.87);
#11807=FILL_AREA_STYLE_COLOUR('',#11806);
#11808=FILL_AREA_STYLE('',(#11807));
#11809=SURFACE_STYLE_FILL_AREA(#11808);
#11810=SURFACE_SIDE_STYLE('',(#11809));
#11811=SURFACE_STYLE_USAGE(.BOTH.,#11810);
#11812=PRESENTATION_STYLE_ASSIGNMENT((#11811));
ENDSEC;
END-ISO-10303-21;
